ISO-10303-21;
HEADER;
/* Generated by software containing ST-Developer
 * from STEP Tools, Inc. (www.steptools.com) 
 */

FILE_DESCRIPTION(
/* description */ ('Belt tensioner idler arm'),
/* implementation_level */ '2;1');

FILE_NAME(
/* name */ 'M4x4 collar screw.step',
/* time_stamp */ '2026-10-28T03:22:15-07:00',
/* author */ (''),
/* organization */ (''),
/* preprocessor_version */ 'ST-DEVELOPER v20.2',
/* originating_system */ 'Autodesk Translation Framework v15.17.0.0',
/* authorisation */ '');

FILE_SCHEMA (('AUTOMOTIVE_DESIGN { 1 0 10303 214 3 1 1 }'));
ENDSEC;

DATA;
#10=MECHANICAL_DESIGN_GEOMETRIC_PRESENTATION_REPRESENTATION('',(#486),#12779);
#311=CONICAL_SURFACE('',#7232,0.185,0.785398163397449);
#410=SHAPE_REPRESENTATION_RELATIONSHIP('SRR','None',#12959,#444);
#444=ADVANCED_BREP_SHAPE_REPRESENTATION('',(#525),#12776);
#486=STYLED_ITEM('',(#13191),#525);
#525=MANIFOLD_SOLID_BREP('Body1',#6223);
#650=FACE_BOUND('',#1623,.T.);
#812=PLANE('',#7221);
#813=PLANE('',#7223);
#814=PLANE('',#7224);
#815=PLANE('',#7225);
#816=PLANE('',#7226);
#817=PLANE('',#7227);
#818=PLANE('',#7228);
#819=PLANE('',#7229);
#820=PLANE('',#7230);
#1124=FACE_OUTER_BOUND('',#1614,.T.);
#1125=FACE_OUTER_BOUND('',#1615,.T.);
#1126=FACE_OUTER_BOUND('',#1616,.T.);
#1127=FACE_OUTER_BOUND('',#1617,.T.);
#1128=FACE_OUTER_BOUND('',#1618,.T.);
#1129=FACE_OUTER_BOUND('',#1619,.T.);
#1130=FACE_OUTER_BOUND('',#1620,.T.);
#1131=FACE_OUTER_BOUND('',#1621,.T.);
#1132=FACE_OUTER_BOUND('',#1622,.T.);
#1133=FACE_OUTER_BOUND('',#1624,.T.);
#1134=FACE_OUTER_BOUND('',#1625,.T.);
#1614=EDGE_LOOP('',(#5236));
#1615=EDGE_LOOP('',(#5237,#5238,#5239,#5240));
#1616=EDGE_LOOP('',(#5241,#5242,#5243,#5244));
#1617=EDGE_LOOP('',(#5245,#5246,#5247,#5248));
#1618=EDGE_LOOP('',(#5249,#5250,#5251,#5252));
#1619=EDGE_LOOP('',(#5253,#5254,#5255,#5256));
#1620=EDGE_LOOP('',(#5257,#5258,#5259,#5260));
#1621=EDGE_LOOP('',(#5261,#5262,#5263,#5264,#5265,#5266));
#1622=EDGE_LOOP('',(#5267));
#1623=EDGE_LOOP('',(#5268,#5269,#5270,#5271,#5272,#5273));
#1624=EDGE_LOOP('',(#5274,#5275,#5276,#5277));
#1625=EDGE_LOOP('',(#5278,#5279,#5280,#5281));
#1963=LINE('',#11957,#2312);
#1964=LINE('',#11959,#2313);
#1965=LINE('',#11961,#2314);
#1966=LINE('',#11962,#2315);
#1967=LINE('',#11965,#2316);
#1968=LINE('',#11967,#2317);
#1969=LINE('',#11968,#2318);
#1970=LINE('',#11971,#2319);
#1971=LINE('',#11973,#2320);
#1972=LINE('',#11974,#2321);
#1973=LINE('',#11977,#2322);
#1974=LINE('',#11979,#2323);
#1975=LINE('',#11980,#2324);
#1976=LINE('',#11983,#2325);
#1977=LINE('',#11985,#2326);
#1978=LINE('',#11986,#2327);
#1979=LINE('',#11988,#2328);
#1980=LINE('',#11989,#2329);
#1981=LINE('',#11997,#2330);
#1982=LINE('',#11999,#2331);
#2312=VECTOR('',#8933,1.);
#2313=VECTOR('',#8934,1.);
#2314=VECTOR('',#8935,1.);
#2315=VECTOR('',#8936,1.);
#2316=VECTOR('',#8939,1.);
#2317=VECTOR('',#8940,1.);
#2318=VECTOR('',#8941,1.);
#2319=VECTOR('',#8944,1.);
#2320=VECTOR('',#8945,1.);
#2321=VECTOR('',#8946,1.);
#2322=VECTOR('',#8949,1.);
#2323=VECTOR('',#8950,1.);
#2324=VECTOR('',#8951,1.);
#2325=VECTOR('',#8954,1.);
#2326=VECTOR('',#8955,1.);
#2327=VECTOR('',#8956,1.);
#2328=VECTOR('',#8959,1.);
#2329=VECTOR('',#8960,1.);
#2330=VECTOR('',#8971,0.185);
#2331=VECTOR('',#8974,0.2);
#2671=CIRCLE('',#7222,0.1954);
#2672=CIRCLE('',#7231,0.17);
#2673=CIRCLE('',#7233,0.1954);
#3154=VERTEX_POINT('',#11952);
#3155=VERTEX_POINT('',#11955);
#3156=VERTEX_POINT('',#11956);
#3157=VERTEX_POINT('',#11958);
#3158=VERTEX_POINT('',#11960);
#3159=VERTEX_POINT('',#11964);
#3160=VERTEX_POINT('',#11966);
#3161=VERTEX_POINT('',#11970);
#3162=VERTEX_POINT('',#11972);
#3163=VERTEX_POINT('',#11976);
#3164=VERTEX_POINT('',#11978);
#3165=VERTEX_POINT('',#11982);
#3166=VERTEX_POINT('',#11984);
#3167=VERTEX_POINT('',#11992);
#3168=VERTEX_POINT('',#11995);
#3873=EDGE_CURVE('',#3154,#3154,#2671,.T.);
#3874=EDGE_CURVE('',#3155,#3156,#1963,.T.);
#3875=EDGE_CURVE('',#3155,#3157,#1964,.T.);
#3876=EDGE_CURVE('',#3157,#3158,#1965,.T.);
#3877=EDGE_CURVE('',#3156,#3158,#1966,.T.);
#3878=EDGE_CURVE('',#3159,#3155,#1967,.T.);
#3879=EDGE_CURVE('',#3159,#3160,#1968,.T.);
#3880=EDGE_CURVE('',#3160,#3157,#1969,.T.);
#3881=EDGE_CURVE('',#3161,#3159,#1970,.T.);
#3882=EDGE_CURVE('',#3161,#3162,#1971,.T.);
#3883=EDGE_CURVE('',#3162,#3160,#1972,.T.);
#3884=EDGE_CURVE('',#3163,#3161,#1973,.T.);
#3885=EDGE_CURVE('',#3163,#3164,#1974,.T.);
#3886=EDGE_CURVE('',#3164,#3162,#1975,.T.);
#3887=EDGE_CURVE('',#3165,#3163,#1976,.T.);
#3888=EDGE_CURVE('',#3165,#3166,#1977,.T.);
#3889=EDGE_CURVE('',#3166,#3164,#1978,.T.);
#3890=EDGE_CURVE('',#3156,#3165,#1979,.T.);
#3891=EDGE_CURVE('',#3158,#3166,#1980,.T.);
#3892=EDGE_CURVE('',#3167,#3167,#2672,.T.);
#3893=EDGE_CURVE('',#3168,#3168,#2673,.T.);
#3894=EDGE_CURVE('',#3168,#3167,#1981,.T.);
#3895=EDGE_CURVE('',#3154,#3168,#1982,.T.);
#5236=ORIENTED_EDGE('',*,*,#3873,.F.);
#5237=ORIENTED_EDGE('',*,*,#3874,.F.);
#5238=ORIENTED_EDGE('',*,*,#3875,.T.);
#5239=ORIENTED_EDGE('',*,*,#3876,.T.);
#5240=ORIENTED_EDGE('',*,*,#3877,.F.);
#5241=ORIENTED_EDGE('',*,*,#3878,.F.);
#5242=ORIENTED_EDGE('',*,*,#3879,.T.);
#5243=ORIENTED_EDGE('',*,*,#3880,.T.);
#5244=ORIENTED_EDGE('',*,*,#3875,.F.);
#5245=ORIENTED_EDGE('',*,*,#3881,.F.);
#5246=ORIENTED_EDGE('',*,*,#3882,.T.);
#5247=ORIENTED_EDGE('',*,*,#3883,.T.);
#5248=ORIENTED_EDGE('',*,*,#3879,.F.);
#5249=ORIENTED_EDGE('',*,*,#3884,.F.);
#5250=ORIENTED_EDGE('',*,*,#3885,.T.);
#5251=ORIENTED_EDGE('',*,*,#3886,.T.);
#5252=ORIENTED_EDGE('',*,*,#3882,.F.);
#5253=ORIENTED_EDGE('',*,*,#3887,.F.);
#5254=ORIENTED_EDGE('',*,*,#3888,.T.);
#5255=ORIENTED_EDGE('',*,*,#3889,.T.);
#5256=ORIENTED_EDGE('',*,*,#3885,.F.);
#5257=ORIENTED_EDGE('',*,*,#3890,.F.);
#5258=ORIENTED_EDGE('',*,*,#3877,.T.);
#5259=ORIENTED_EDGE('',*,*,#3891,.T.);
#5260=ORIENTED_EDGE('',*,*,#3888,.F.);
#5261=ORIENTED_EDGE('',*,*,#3891,.F.);
#5262=ORIENTED_EDGE('',*,*,#3876,.F.);
#5263=ORIENTED_EDGE('',*,*,#3880,.F.);
#5264=ORIENTED_EDGE('',*,*,#3883,.F.);
#5265=ORIENTED_EDGE('',*,*,#3886,.F.);
#5266=ORIENTED_EDGE('',*,*,#3889,.F.);
#5267=ORIENTED_EDGE('',*,*,#3892,.F.);
#5268=ORIENTED_EDGE('',*,*,#3874,.T.);
#5269=ORIENTED_EDGE('',*,*,#3890,.T.);
#5270=ORIENTED_EDGE('',*,*,#3887,.T.);
#5271=ORIENTED_EDGE('',*,*,#3884,.T.);
#5272=ORIENTED_EDGE('',*,*,#3881,.T.);
#5273=ORIENTED_EDGE('',*,*,#3878,.T.);
#5274=ORIENTED_EDGE('',*,*,#3893,.F.);
#5275=ORIENTED_EDGE('',*,*,#3894,.T.);
#5276=ORIENTED_EDGE('',*,*,#3892,.T.);
#5277=ORIENTED_EDGE('',*,*,#3894,.F.);
#5278=ORIENTED_EDGE('',*,*,#3873,.T.);
#5279=ORIENTED_EDGE('',*,*,#3895,.T.);
#5280=ORIENTED_EDGE('',*,*,#3893,.T.);
#5281=ORIENTED_EDGE('',*,*,#3895,.F.);
#5763=CYLINDRICAL_SURFACE('',#7234,0.1954);
#6101=ADVANCED_FACE('',(#1124),#812,.F.);
#6102=ADVANCED_FACE('',(#1125),#813,.F.);
#6103=ADVANCED_FACE('',(#1126),#814,.F.);
#6104=ADVANCED_FACE('',(#1127),#815,.F.);
#6105=ADVANCED_FACE('',(#1128),#816,.F.);
#6106=ADVANCED_FACE('',(#1129),#817,.F.);
#6107=ADVANCED_FACE('',(#1130),#818,.F.);
#6108=ADVANCED_FACE('',(#1131),#819,.F.);
#6109=ADVANCED_FACE('',(#1132,#650),#820,.T.);
#6110=ADVANCED_FACE('',(#1133),#311,.T.);
#6111=ADVANCED_FACE('',(#1134),#5763,.T.);
#6223=CLOSED_SHELL('',(#6101,#6102,#6103,#6104,#6105,#6106,#6107,#6108,
#6109,#6110,#6111));
#7220=AXIS2_PLACEMENT_3D('',#11950,#8925,#8926);
#7221=AXIS2_PLACEMENT_3D('',#11951,#8927,#8928);
#7222=AXIS2_PLACEMENT_3D('',#11953,#8929,#8930);
#7223=AXIS2_PLACEMENT_3D('',#11954,#8931,#8932);
#7224=AXIS2_PLACEMENT_3D('',#11963,#8937,#8938);
#7225=AXIS2_PLACEMENT_3D('',#11969,#8942,#8943);
#7226=AXIS2_PLACEMENT_3D('',#11975,#8947,#8948);
#7227=AXIS2_PLACEMENT_3D('',#11981,#8952,#8953);
#7228=AXIS2_PLACEMENT_3D('',#11987,#8957,#8958);
#7229=AXIS2_PLACEMENT_3D('',#11990,#8961,#8962);
#7230=AXIS2_PLACEMENT_3D('',#11991,#8963,#8964);
#7231=AXIS2_PLACEMENT_3D('',#11993,#8965,#8966);
#7232=AXIS2_PLACEMENT_3D('',#11994,#8967,#8968);
#7233=AXIS2_PLACEMENT_3D('',#11996,#8969,#8970);
#7234=AXIS2_PLACEMENT_3D('',#11998,#8972,#8973);
#8925=DIRECTION('axis',(0.,0.,1.));
#8926=DIRECTION('refdir',(1.,0.,0.));
#8927=DIRECTION('center_axis',(0.,1.,0.));
#8928=DIRECTION('ref_axis',(1.,0.,0.));
#8929=DIRECTION('center_axis',(0.,1.,0.));
#8930=DIRECTION('ref_axis',(1.,0.,0.));
#8931=DIRECTION('center_axis',(0.866025403784439,0.,-0.5));
#8932=DIRECTION('ref_axis',(0.5,0.,0.866025403784439));
#8933=DIRECTION('',(0.5,0.,0.866025403784439));
#8934=DIRECTION('',(0.,-1.,0.));
#8935=DIRECTION('',(0.5,0.,0.866025403784439));
#8936=DIRECTION('',(0.,-1.,0.));
#8937=DIRECTION('center_axis',(1.20185167898973E-16,0.,-1.));
#8938=DIRECTION('ref_axis',(1.,0.,1.20185167898973E-16));
#8939=DIRECTION('',(1.,0.,1.20185167898973E-16));
#8940=DIRECTION('',(0.,-1.,0.));
#8941=DIRECTION('',(1.,0.,1.20185167898973E-16));
#8942=DIRECTION('center_axis',(-0.866025403784439,0.,-0.5));
#8943=DIRECTION('ref_axis',(0.5,0.,-0.866025403784439));
#8944=DIRECTION('',(0.5,0.,-0.866025403784439));
#8945=DIRECTION('',(0.,-1.,0.));
#8946=DIRECTION('',(0.5,0.,-0.866025403784439));
#8947=DIRECTION('center_axis',(-0.866025403784439,0.,0.5));
#8948=DIRECTION('ref_axis',(-0.5,0.,-0.866025403784439));
#8949=DIRECTION('',(-0.5,0.,-0.866025403784439));
#8950=DIRECTION('',(0.,-1.,0.));
#8951=DIRECTION('',(-0.5,0.,-0.866025403784439));
#8952=DIRECTION('center_axis',(-2.40370335797945E-16,0.,1.));
#8953=DIRECTION('ref_axis',(-1.,0.,-2.40370335797945E-16));
#8954=DIRECTION('',(-1.,0.,-2.40370335797945E-16));
#8955=DIRECTION('',(0.,-1.,0.));
#8956=DIRECTION('',(-1.,0.,-2.40370335797945E-16));
#8957=DIRECTION('center_axis',(0.866025403784439,0.,0.5));
#8958=DIRECTION('ref_axis',(-0.5,0.,0.866025403784439));
#8959=DIRECTION('',(-0.5,0.,0.866025403784439));
#8960=DIRECTION('',(-0.5,0.,0.866025403784439));
#8961=DIRECTION('center_axis',(0.,-1.,0.));
#8962=DIRECTION('ref_axis',(0.,0.,-1.));
#8963=DIRECTION('center_axis',(0.,1.,0.));
#8964=DIRECTION('ref_axis',(0.,0.,1.));
#8965=DIRECTION('center_axis',(0.,-1.,0.));
#8966=DIRECTION('ref_axis',(1.,0.,0.));
#8967=DIRECTION('center_axis',(0.,-1.,0.));
#8968=DIRECTION('ref_axis',(1.,0.,0.));
#8969=DIRECTION('center_axis',(0.,-1.,0.));
#8970=DIRECTION('ref_axis',(1.,0.,0.));
#8971=DIRECTION('',(0.707106781186548,0.707106781186547,8.65956056235494E-17));
#8972=DIRECTION('center_axis',(0.,-1.,0.));
#8973=DIRECTION('ref_axis',(1.,0.,0.));
#8974=DIRECTION('',(0.,1.,0.));
#11950=CARTESIAN_POINT('',(0.,0.,0.));
#11951=CARTESIAN_POINT('Origin',(0.,-0.4,0.));
#11952=CARTESIAN_POINT('',(-0.1954,-0.4,2.39295984553393E-17));
#11953=CARTESIAN_POINT('Origin',(0.,-0.4,0.));
#11954=CARTESIAN_POINT('Origin',(0.0577350269189626,0.,-0.1));
#11955=CARTESIAN_POINT('',(0.0577350269189626,0.,-0.1));
#11956=CARTESIAN_POINT('',(0.115470053837925,0.,0.));
#11957=CARTESIAN_POINT('',(0.0934187836487032,0.,-0.0381939203391614));
#11958=CARTESIAN_POINT('',(0.0577350269189626,-0.2,-0.1));
#11959=CARTESIAN_POINT('',(0.0577350269189626,0.,-0.1));
#11960=CARTESIAN_POINT('',(0.115470053837925,-0.2,0.));
#11961=CARTESIAN_POINT('',(0.115470053837925,-0.2,0.));
#11962=CARTESIAN_POINT('',(0.115470053837925,0.,0.));
#11963=CARTESIAN_POINT('Origin',(-0.0577350269189626,0.,-0.1));
#11964=CARTESIAN_POINT('',(-0.0577350269189626,0.,-0.1));
#11965=CARTESIAN_POINT('',(0.0561324865405187,0.,-0.1));
#11966=CARTESIAN_POINT('',(-0.0577350269189626,-0.2,-0.1));
#11967=CARTESIAN_POINT('',(-0.0577350269189626,0.,-0.1));
#11968=CARTESIAN_POINT('',(0.0577350269189626,-0.2,-0.1));
#11969=CARTESIAN_POINT('Origin',(-0.115470053837925,0.,-1.38777878078145E-17));
#11970=CARTESIAN_POINT('',(-0.115470053837925,0.,-1.41410031829988E-17));
#11971=CARTESIAN_POINT('',(-0.0797862971081845,0.,-0.0618060796608387));
#11972=CARTESIAN_POINT('',(-0.115470053837925,-0.2,-1.38777878078145E-17));
#11973=CARTESIAN_POINT('',(-0.115470053837925,0.,-1.41410031829988E-17));
#11974=CARTESIAN_POINT('',(-0.0577350269189626,-0.2,-0.1));
#11975=CARTESIAN_POINT('Origin',(-0.0577350269189626,0.,0.1));
#11976=CARTESIAN_POINT('',(-0.0577350269189626,0.,0.1));
#11977=CARTESIAN_POINT('',(-0.0509187836487033,0.,0.111806079660839));
#11978=CARTESIAN_POINT('',(-0.0577350269189626,-0.2,0.1));
#11979=CARTESIAN_POINT('',(-0.0577350269189626,0.,0.1));
#11980=CARTESIAN_POINT('',(-0.115470053837925,-0.2,-1.41410031829988E-17));
#11981=CARTESIAN_POINT('Origin',(0.0577350269189626,0.,0.1));
#11982=CARTESIAN_POINT('',(0.0577350269189626,0.,0.1));
#11983=CARTESIAN_POINT('',(0.113867513459481,0.,0.1));
#11984=CARTESIAN_POINT('',(0.0577350269189626,-0.2,0.1));
#11985=CARTESIAN_POINT('',(0.0577350269189626,0.,0.1));
#11986=CARTESIAN_POINT('',(-0.0577350269189626,-0.2,0.1));
#11987=CARTESIAN_POINT('Origin',(0.115470053837925,0.,0.));
#11988=CARTESIAN_POINT('',(0.122286297108185,0.,-0.0118060796608386));
#11989=CARTESIAN_POINT('',(0.0577350269189626,-0.2,0.1));
#11990=CARTESIAN_POINT('Origin',(0.,-0.2,0.));
#11991=CARTESIAN_POINT('Origin',(0.17,0.,0.));
#11992=CARTESIAN_POINT('',(-0.17,-8.67361737988404E-18,-2.0818995585505E-17));
#11993=CARTESIAN_POINT('Origin',(0.,0.,0.));
#11994=CARTESIAN_POINT('Origin',(0.,-0.015,0.));
#11995=CARTESIAN_POINT('',(-0.1954,-0.0254,-2.39295984553393E-17));
#11996=CARTESIAN_POINT('Origin',(0.,-0.0254,0.));
#11997=CARTESIAN_POINT('',(-0.185,-0.015,-2.2655965784226E-17));
#11998=CARTESIAN_POINT('Origin',(0.,-0.2775,0.));
#11999=CARTESIAN_POINT('',(-0.1954,-0.2775,-2.39295984553393E-17));
#12736=UNCERTAINTY_MEASURE_WITH_UNIT(LENGTH_MEASURE(0.001),#12780,
'DISTANCE_ACCURACY_VALUE',
'Maximum model space distance between geometric entities at asserted c
onnectivities');
#12739=UNCERTAINTY_MEASURE_WITH_UNIT(LENGTH_MEASURE(0.001),#12780,
'DISTANCE_ACCURACY_VALUE',
'Maximum model space distance between geometric entities at asserted c
onnectivities');
#12776=(
GEOMETRIC_REPRESENTATION_CONTEXT(3)
GLOBAL_UNCERTAINTY_ASSIGNED_CONTEXT((#12736))
GLOBAL_UNIT_ASSIGNED_CONTEXT((#12780,#12782,#12783))
REPRESENTATION_CONTEXT('','3D')
);
#12779=(
GEOMETRIC_REPRESENTATION_CONTEXT(3)
GLOBAL_UNCERTAINTY_ASSIGNED_CONTEXT((#12739))
GLOBAL_UNIT_ASSIGNED_CONTEXT((#12780,#12782,#12783))
REPRESENTATION_CONTEXT('','3D')
);
#12780=(
LENGTH_UNIT()
NAMED_UNIT(*)
SI_UNIT(.CENTI.,.METRE.)
);
#12782=(
NAMED_UNIT(*)
PLANE_ANGLE_UNIT()
SI_UNIT($,.RADIAN.)
);
#12783=(
NAMED_UNIT(*)
SI_UNIT($,.STERADIAN.)
SOLID_ANGLE_UNIT()
);
#12820=SHAPE_DEFINITION_REPRESENTATION(#12888,#12959);
#12888=PRODUCT_DEFINITION_SHAPE('',$,#12999);
#12959=SHAPE_REPRESENTATION('',(#7220),#12776);
#12962=PRODUCT_DEFINITION_CONTEXT('part definition',#13081,'design');
#12999=PRODUCT_DEFINITION('M4x4 collar screw','M4x4 collar screw',#13038,
#12962);
#13038=PRODUCT_DEFINITION_FORMATION('',$,#13119);
#13081=APPLICATION_CONTEXT(
'Core Data for Automotive Mechanical Design Process');
#13082=PRODUCT_CONTEXT('part definition',#13081,'mechanical');
#13119=PRODUCT('M4x4 collar screw','M4x4 collar screw',
'M4x4 collar screw',(#13082));
#13185=COLOUR_RGB('Black',0.12,0.14,0.17);
#13186=FILL_AREA_STYLE_COLOUR('',#13185);
#13187=FILL_AREA_STYLE('',(#13186));
#13188=SURFACE_STYLE_FILL_AREA(#13187);
#13189=SURFACE_SIDE_STYLE('',(#13188));
#13190=SURFACE_STYLE_USAGE(.BOTH.,#13189);
#13191=PRESENTATION_STYLE_ASSIGNMENT((#13190));
ENDSEC;
END-ISO-10303-21;
